ISO-10303-21;
HEADER;
FILE_DESCRIPTION (('STEP AP214'),
    '1' );
FILE_NAME ('socket button head screw_iso_ISO 7380 - M4 x 10 - 10N.step',
    '2026-10-19T14:05:14',
    ( '' ),
    ( '' ),
    'SwSTEP 2.0',
    'SolidWorks 2025',
    '' );
FILE_SCHEMA (( 'AUTOMOTIVE_DESIGN' ));
ENDSEC;

DATA;
#4=DIRECTION ( 'NONE',  ( 1.000000000000000000, 0.000000000000000000, -0.000000000000000000 ) ) ;
#12=ORIENTED_EDGE ( 'NONE', *, *, #8842, .T. ) ;
#21=MECHANICAL_DESIGN_GEOMETRIC_PRESENTATION_REPRESENTATION('',(#1599),#7104);
#34=ADVANCED_FACE ( 'NONE', ( #5878 ), #8015, .T. ) ;
#42=CARTESIAN_POINT ( 'NONE',  ( 1.300000000000000044, -0.7216878364870317197, -1.250000000000000000 ) ) ;
#43=CYLINDRICAL_SURFACE ( 'NONE', #4602, 1.999999999999999556 ) ;
#46=DIRECTION ( 'NONE',  ( -0.000000000000000000, 0.000000000000000000, 1.000000000000000000 ) ) ;
#50=DIRECTION ( 'NONE',  ( 0.000000000000000000, 0.000000000000000000, 1.000000000000000000 ) ) ;
#81=EDGE_LOOP ( 'NONE', ( #9222, #5342, #9321, #2491 ) ) ;
#84=AXIS2_PLACEMENT_3D ( 'NONE', #4346, #782, #3690 ) ;
#94=DIRECTION ( 'NONE',  ( -0.000000000000000000, -0.5000000000000001110, -0.8660254037844385966 ) ) ;
#102=VECTOR ( 'NONE', #2807, 1000.000000000000000 ) ;
#109=AXIS2_PLACEMENT_3D ( 'NONE', #9198, #4705, #305 ) ;
#128=ORIENTED_EDGE ( 'NONE', *, *, #8520, .F. ) ;
#138=FACE_OUTER_BOUND ( 'NONE', #6010, .T. ) ;
#148=DIRECTION ( 'NONE',  ( 0.000000000000000000, 0.000000000000000000, -1.000000000000000000 ) ) ;
#160=AXIS2_PLACEMENT_3D ( 'NONE', #5562, #8483, #3937 ) ;
#169=EDGE_CURVE ( 'NONE', #2001, #9443, #8039, .T. ) ;
#170=ORIENTED_EDGE ( 'NONE', *, *, #4564, .F. ) ;
#171=VECTOR ( 'NONE', #8479, 1000.000000000000000 ) ;
#176=VECTOR ( 'NONE', #6148, 1000.000000000000000 ) ;
#199=DIRECTION ( 'NONE',  ( 0.000000000000000000, 0.000000000000000000, 1.000000000000000000 ) ) ;
#205=ORIENTED_EDGE ( 'NONE', *, *, #694, .T. ) ;
#210=CARTESIAN_POINT ( 'NONE',  ( 12.20000000000000107, 0.000000000000000000, 0.000000000000000000 ) ) ;
#212=DIRECTION ( 'NONE',  ( 0.000000000000000000, 0.000000000000000000, 1.000000000000000000 ) ) ;
#235=EDGE_CURVE ( 'NONE', #6362, #4125, #4927, .T. ) ;
#254=CARTESIAN_POINT ( 'NONE',  ( 1.820000000000000062, 0.000000000000000000, 0.000000000000000000 ) ) ;
#261=VECTOR ( 'NONE', #1095, 1000.000000000000114 ) ;
#262=VECTOR ( 'NONE', #9116, 1000.000000000000114 ) ;
#273=EDGE_CURVE ( 'NONE', #4125, #4231, #5470, .T. ) ;
#278=DIRECTION ( 'NONE',  ( 0.000000000000000000, 0.000000000000000000, 1.000000000000000000 ) ) ;
#305=DIRECTION ( 'NONE',  ( 0.000000000000000000, 0.000000000000000000, 1.000000000000000000 ) ) ;
#320=CIRCLE ( 'NONE', #5041, 3.799999999999999378 ) ;
#329=CARTESIAN_POINT ( 'NONE',  ( 1.300000000000000044, -1.443375672974064328, -9.326206579303807412E-18 ) ) ;
#391=ORIENTED_EDGE ( 'NONE', *, *, #2229, .T. ) ;
#398=AXIS2_PLACEMENT_3D ( 'NONE', #7354, #1376, #6045 ) ;
#399=CIRCLE ( 'NONE', #2107, 2.199999999999999734 ) ;
#412=EDGE_CURVE ( 'NONE', #8367, #8213, #1224, .T. ) ;
#414=AXIS2_PLACEMENT_3D ( 'NONE', #5920, #5869, #2063 ) ;
#416=CARTESIAN_POINT ( 'NONE',  ( 2.021687836487040535, 2.655529440325959183E-32, -2.168404344971008868E-16 ) ) ;
#417=AXIS2_PLACEMENT_3D ( 'NONE', #6684, #4224, #278 ) ;
#425=CARTESIAN_POINT ( 'NONE',  ( 1.300000000000000044, 0.000000000000000000, 0.000000000000000000 ) ) ;
#436=PRODUCT_DEFINITION ( 'UNKNOWN', '', #6631, #7162 ) ;
#461=DIRECTION ( 'NONE',  ( -1.000000000000000000, -0.000000000000000000, -0.000000000000000000 ) ) ;
#485=CARTESIAN_POINT ( 'NONE',  ( 2.400000000000000799, 0.000000000000000000, 0.000000000000000000 ) ) ;
#490=SHAPE_REPRESENTATION ( 'socket button head screw_iso_ISO 7380 - M4 x 10 - 10N', ( #6314 ), #6474 ) ;
#492=AXIS2_PLACEMENT_3D ( 'NONE', #3896, #148, #8677 ) ;
#515=CARTESIAN_POINT ( 'NONE',  ( 3.885274725274726393, -8.673617379884035472E-16, 0.000000000000000000 ) ) ;
#559=CARTESIAN_POINT ( 'NONE',  ( 2.400000000000000799, 0.000000000000000000, 0.000000000000000000 ) ) ;
#562=ORIENTED_EDGE ( 'NONE', *, *, #6925, .F. ) ;
#572=FACE_OUTER_BOUND ( 'NONE', #3011, .T. ) ;
#597=DIRECTION ( 'NONE',  ( -1.000000000000000000, -0.000000000000000000, -0.000000000000000000 ) ) ;
#601=EDGE_LOOP ( 'NONE', ( #1791, #2540, #7807, #3145, #4063 ) ) ;
#603=DIRECTION ( 'NONE',  ( 0.000000000000000000, 0.000000000000000000, 1.000000000000000000 ) ) ;
#607=EDGE_LOOP ( 'NONE', ( #895, #6657 ) ) ;
#633=CARTESIAN_POINT ( 'NONE',  ( 0.000000000000000000, -1.443375672974064328, -9.326206579303807412E-18 ) ) ;
#638=LINE ( 'NONE', #8740, #6512 ) ;
#656=EDGE_LOOP ( 'NONE', ( #2206, #5652, #8813, #128, #3194 ) ) ;
#664=LINE ( 'NONE', #4320, #1771 ) ;
#668=EDGE_CURVE ( 'NONE', #2236, #5750, #3130, .T. ) ;
#680=DIRECTION ( 'NONE',  ( 0.000000000000000000, 0.000000000000000000, 1.000000000000000000 ) ) ;
#682=CIRCLE ( 'NONE', #6188, 2.000000000000000000 ) ;
#694=EDGE_CURVE ( 'NONE', #9443, #2001, #5462, .T. ) ;
#696=CARTESIAN_POINT ( 'NONE',  ( 1.300000000000000044, 0.7216878364870328300, 1.250000000000000000 ) ) ;
#700=ORIENTED_EDGE ( 'NONE', *, *, #4695, .T. ) ;
#714=DIRECTION ( 'NONE',  ( 1.000000000000000000, 0.000000000000000000, 0.000000000000000000 ) ) ;
#718=ORIENTED_EDGE ( 'NONE', *, *, #3473, .F. ) ;
#728=CARTESIAN_POINT ( 'NONE',  ( 11.80999999999999872, 0.000000000000000000, 0.000000000000000000 ) ) ;
#737=LINE ( 'NONE', #9449, #1576 ) ;
#782=DIRECTION ( 'NONE',  ( 0.000000000000000000, 1.224646799147353207E-16, -1.000000000000000000 ) ) ;
#787=ORIENTED_EDGE ( 'NONE', *, *, #1184, .T. ) ;
#803=VECTOR ( 'NONE', #7890, 1000.000000000000000 ) ;
#816=AXIS2_PLACEMENT_3D ( 'NONE', #3083, #4481, #2339 ) ;
#866=ORIENTED_EDGE ( 'NONE', *, *, #4695, .F. ) ;
#869=CARTESIAN_POINT ( 'NONE',  ( 1.300000000000000044, 3.252606517456513302E-16, 2.499999999999999556 ) ) ;
#879=VECTOR ( 'NONE', #5666, 1000.000000000000114 ) ;
#895=ORIENTED_EDGE ( 'NONE', *, *, #4487, .F. ) ;
#928=VERTEX_POINT ( 'NONE', #8770 ) ;
#931=FACE_OUTER_BOUND ( 'NONE', #1919, .T. ) ;
#933=LINE ( 'NONE', #3195, #5567 ) ;
#940=CARTESIAN_POINT ( 'NONE',  ( 1.300000000000000044, 0.000000000000000000, -1.250000000000000000 ) ) ;
#952=EDGE_CURVE ( 'NONE', #3643, #6132, #8814, .T. ) ;
#978=DIRECTION ( 'NONE',  ( -1.000000000000000000, -0.000000000000000000, -0.000000000000000000 ) ) ;
#1011=DIRECTION ( 'NONE',  ( -0.000000000000000000, 1.000000000000000000, -0.000000000000000000 ) ) ;
#1012=EDGE_CURVE ( 'NONE', #6132, #8213, #638, .T. ) ;
#1013=ORIENTED_EDGE ( 'NONE', *, *, #1538, .T. ) ;
#1022=( NAMED_UNIT ( * ) SI_UNIT ( $, .STERADIAN. ) SOLID_ANGLE_UNIT ( ) );
#1031=AXIS2_PLACEMENT_3D ( 'NONE', #425, #5648, #3423 ) ;
#1086=ORIENTED_EDGE ( 'NONE', *, *, #668, .F. ) ;
#1095=DIRECTION ( 'NONE',  ( -0.5000000000000044409, 1.060575238724903587E-16, -0.8660254037844360431 ) ) ;
#1145=ORIENTED_EDGE ( 'NONE', *, *, #9427, .T. ) ;
#1184=EDGE_CURVE ( 'NONE', #8659, #1276, #737, .T. ) ;
#1190=ORIENTED_EDGE ( 'NONE', *, *, #8776, .F. ) ;
#1209=ORIENTED_EDGE ( 'NONE', *, *, #412, .T. ) ;
#1224=CIRCLE ( 'NONE', #4519, 1.999999999999999556 ) ;
#1229=CARTESIAN_POINT ( 'NONE',  ( 1.300000000000000044, 0.7216878364870328300, 1.250000000000000000 ) ) ;
#1249=EDGE_CURVE ( 'NONE', #928, #9118, #4279, .T. ) ;
#1276=VERTEX_POINT ( 'NONE', #5015 ) ;
#1316=FACE_OUTER_BOUND ( 'NONE', #2423, .T. ) ;
#1324=CARTESIAN_POINT ( 'NONE',  ( 1.820000000000000062, 4.653657836759941744E-16, -3.799999999999999378 ) ) ;
#1333=CIRCLE ( 'NONE', #398, 2.199999999999999734 ) ;
#1337=ORIENTED_EDGE ( 'NONE', *, *, #7754, .F. ) ;
#1358=VERTEX_POINT ( 'NONE', #3478 ) ;
#1364=CARTESIAN_POINT ( 'NONE',  ( 0.000000000000000000, -0.7216878364870318308, 1.250000000000000000 ) ) ;
#1374=DIRECTION ( 'NONE',  ( 0.000000000000000000, -1.000000000000000000, 0.000000000000000000 ) ) ;
#1376=DIRECTION ( 'NONE',  ( -1.000000000000000000, -0.000000000000000000, -0.000000000000000000 ) ) ;
#1406=CONICAL_SURFACE ( 'NONE', #160, 1732.050807568856271, 1.047197551196592524 ) ;
#1413=DIRECTION ( 'NONE',  ( -1.000000000000000000, 0.000000000000000000, -0.000000000000000000 ) ) ;
#1414=CARTESIAN_POINT ( 'NONE',  ( 2.400000000000000799, 0.000000000000000000, 2.199999999999999734 ) ) ;
#1431=CYLINDRICAL_SURFACE ( 'NONE', #414, 1.999999999999999556 ) ;
#1452=AXIS2_PLACEMENT_3D ( 'NONE', #5249, #8260, #4518 ) ;
#1459=CARTESIAN_POINT ( 'NONE',  ( 12.20000000000000107, 0.000000000000000000, 0.000000000000000000 ) ) ;
#1463=CIRCLE ( 'NONE', #6506, 1.899999999999999689 ) ;
#1473=EDGE_CURVE ( 'NONE', #6406, #6663, #8319, .T. ) ;
#1508=AXIS2_PLACEMENT_3D ( 'NONE', #9599, #2269, #6957 ) ;
#1516=AXIS2_PLACEMENT_3D ( 'NONE', #3381, #3570, #9421 ) ;
#1523=CARTESIAN_POINT ( 'NONE',  ( 1.820000000000000062, 0.000000000000000000, 0.000000000000000000 ) ) ;
#1538=EDGE_CURVE ( 'NONE', #928, #8583, #4199, .T. ) ;
#1551=ORIENTED_EDGE ( 'NONE', *, *, #5337, .F. ) ;
#1552=CARTESIAN_POINT ( 'NONE',  ( 1.300000000000000044, -0.7216878364870317197, -1.250000000000000000 ) ) ;
#1563=DIRECTION ( 'NONE',  ( 1.000000000000000000, 0.000000000000000000, 0.000000000000000000 ) ) ;
#1576=VECTOR ( 'NONE', #3746, 1000.000000000000114 ) ;
#1577=PRODUCT_DEFINITION_SHAPE ( 'NONE', 'NONE',  #436 ) ;
#1579=CARTESIAN_POINT ( 'NONE',  ( 0.000000000000000000, 0.000000000000000000, 1.999999999999999556 ) ) ;
#1595=VERTEX_POINT ( 'NONE', #5690 ) ;
#1599=STYLED_ITEM('',(#9799),#9696);
#1649=CIRCLE ( 'NONE', #7164, 1.999999999999999556 ) ;
#1667=AXIS2_PLACEMENT_3D ( 'NONE', #559, #6652, #603 ) ;
#1680=EDGE_LOOP ( 'NONE', ( #6037, #5607, #3662 ) ) ;
#1702=LINE ( 'NONE', #7586, #6807 ) ;
#1712=ORIENTED_EDGE ( 'NONE', *, *, #6925, .T. ) ;
#1728=AXIS2_PLACEMENT_3D ( 'NONE', #515, #3511, #6519 ) ;
#1732=PLANE ( 'NONE',  #9087 ) ;
#1733=ORIENTED_EDGE ( 'NONE', *, *, #5337, .T. ) ;
#1738=DIRECTION ( 'NONE',  ( -1.000000000000000000, -0.000000000000000000, -0.000000000000000000 ) ) ;
#1758=CIRCLE ( 'NONE', #5240, 1.249999999999999778 ) ;
#1771=VECTOR ( 'NONE', #2872, 1000.000000000000000 ) ;
#1791=ORIENTED_EDGE ( 'NONE', *, *, #3717, .F. ) ;
#1809=VECTOR ( 'NONE', #2463, 1000.000000000000114 ) ;
#1812=ORIENTED_EDGE ( 'NONE', *, *, #1538, .F. ) ;
#1834=CIRCLE ( 'NONE', #1516, 1.249999999999999778 ) ;
#1838=AXIS2_PLACEMENT_3D ( 'NONE', #254, #7042, #7244 ) ;
#1894=SPHERICAL_SURFACE ( 'NONE', #5678, 4.324969328314201888 ) ;
#1919=EDGE_LOOP ( 'NONE', ( #6865, #4567, #9685, #12, #6940 ) ) ;
#1940=CARTESIAN_POINT ( 'NONE',  ( 1.300000000000000044, 3.252606517456513302E-16, 2.499999999999999556 ) ) ;
#1942=DIRECTION ( 'NONE',  ( 0.000000000000000000, 1.000000000000000000, 0.000000000000000000 ) ) ;
#1950=EDGE_CURVE ( 'NONE', #9118, #8659, #2607, .T. ) ;
#1952=CIRCLE ( 'NONE', #84, 4.324969328314201888 ) ;
#1965=ADVANCED_FACE ( 'NONE', ( #8503 ), #1732, .T. ) ;
#1982=AXIS2_PLACEMENT_3D ( 'NONE', #7594, #3936, #7785 ) ;
#1988=EDGE_CURVE ( 'NONE', #6362, #8659, #4361, .T. ) ;
#2001=VERTEX_POINT ( 'NONE', #3956 ) ;
#2024=EDGE_LOOP ( 'NONE', ( #205, #7432, #6216, #6428, #3410 ) ) ;
#2036=CARTESIAN_POINT ( 'NONE',  ( 1.300000000000000044, 1.443375672974065216, 1.084202172492522584E-16 ) ) ;
#2063=DIRECTION ( 'NONE',  ( 0.000000000000000000, 0.000000000000000000, 1.000000000000000000 ) ) ;
#2081=EDGE_CURVE ( 'NONE', #4551, #7854, #399, .T. ) ;
#2095=CARTESIAN_POINT ( 'NONE',  ( 1.300000000000000044, -1.443375672974064328, -9.326206579303807412E-18 ) ) ;
#2107=AXIS2_PLACEMENT_3D ( 'NONE', #2753, #597, #2800 ) ;
#2132=CIRCLE ( 'NONE', #1982, 1.249999999999999778 ) ;
#2143=DIRECTION ( 'NONE',  ( 0.000000000000000000, 0.000000000000000000, 1.000000000000000000 ) ) ;
#2149=DIRECTION ( 'NONE',  ( 0.000000000000000000, 0.000000000000000000, -1.000000000000000000 ) ) ;
#2150=FACE_OUTER_BOUND ( 'NONE', #3206, .T. ) ;
#2163=EDGE_LOOP ( 'NONE', ( #1551, #7027, #1812 ) ) ;
#2185=CARTESIAN_POINT ( 'NONE',  ( 12.20000000000000107, 0.000000000000000000, 0.000000000000000000 ) ) ;
#2206=ORIENTED_EDGE ( 'NONE', *, *, #1473, .T. ) ;
#2212=PLANE ( 'NONE',  #1452 ) ;
#2221=CARTESIAN_POINT ( 'NONE',  ( 12.20000000000000107, 2.210487472460972698E-16, -1.610000000000000098 ) ) ;
#2229=EDGE_CURVE ( 'NONE', #8766, #7406, #3059, .T. ) ;
#2236=VERTEX_POINT ( 'NONE', #6845 ) ;
#2239=EDGE_CURVE ( 'NONE', #8213, #8367, #1649, .T. ) ;
#2269=DIRECTION ( 'NONE',  ( -1.000000000000000000, -0.000000000000000000, -0.000000000000000000 ) ) ;
#2272=EDGE_LOOP ( 'NONE', ( #2565, #2344 ) ) ;
#2285=VECTOR ( 'NONE', #9290, 1000.000000000000114 ) ;
#2287=ORIENTED_EDGE ( 'NONE', *, *, #7774, .T. ) ;
#2295=FACE_OUTER_BOUND ( 'NONE', #5394, .T. ) ;
#2309=DIRECTION ( 'NONE',  ( -0.000000000000000000, 0.5000000000000002220, -0.8660254037844384856 ) ) ;
#2312=ORIENTED_EDGE ( 'NONE', *, *, #7743, .F. ) ;
#2321=ORIENTED_EDGE ( 'NONE', *, *, #9459, .T. ) ;
#2333=CARTESIAN_POINT ( 'NONE',  ( 1.300000000000000044, 0.000000000000000000, 1.249999999999999778 ) ) ;
#2339=DIRECTION ( 'NONE',  ( 0.000000000000000000, 0.000000000000000000, 1.000000000000000000 ) ) ;
#2343=CARTESIAN_POINT ( 'NONE',  ( 1.300000000000000044, 0.7216878364870328300, -1.250000000000000000 ) ) ;
#2344=ORIENTED_EDGE ( 'NONE', *, *, #169, .F. ) ;
#2350=PRODUCT ( 'socket button head screw_iso_ISO 7380 - M4 x 10 - 10N', 'socket button head screw_iso_ISO 7380 - M4 x 10 - 10N', '', ( #9735 ) ) ;
#2359=ORIENTED_EDGE ( 'NONE', *, *, #5778, .T. ) ;
#2367=ORIENTED_EDGE ( 'NONE', *, *, #1249, .F. ) ;
#2379=PLANE ( 'NONE',  #4488 ) ;
#2380=DIRECTION ( 'NONE',  ( 0.000000000000000000, 0.000000000000000000, 1.000000000000000000 ) ) ;
#2395=FACE_OUTER_BOUND ( 'NONE', #656, .T. ) ;
#2403=ADVANCED_FACE ( 'NONE', ( #931 ), #7483, .F. ) ;
#2423=EDGE_LOOP ( 'NONE', ( #5063, #9323, #1190 ) ) ;
#2447=VECTOR ( 'NONE', #94, 1000.000000000000000 ) ;
#2452=ORIENTED_EDGE ( 'NONE', *, *, #1988, .T. ) ;
#2455=ORIENTED_EDGE ( 'NONE', *, *, #3473, .T. ) ;
#2463=DIRECTION ( 'NONE',  ( -0.000000000000000000, 0.5000000000000002220, -0.8660254037844384856 ) ) ;
#2488=EDGE_CURVE ( 'NONE', #4231, #6406, #3393, .T. ) ;
#2491=ORIENTED_EDGE ( 'NONE', *, *, #9609, .F. ) ;
#2507=VECTOR ( 'NONE', #6731, 1000.000000000000227 ) ;
#2523=ADVANCED_FACE ( 'NONE', ( #5670 ), #7897, .T. ) ;
#2524=ORIENTED_EDGE ( 'NONE', *, *, #668, .T. ) ;
#2540=ORIENTED_EDGE ( 'NONE', *, *, #169, .T. ) ;
#2565=ORIENTED_EDGE ( 'NONE', *, *, #694, .F. ) ;
#2573=FACE_OUTER_BOUND ( 'NONE', #2163, .T. ) ;
#2585=FACE_OUTER_BOUND ( 'NONE', #81, .T. ) ;
#2592=DIRECTION ( 'NONE',  ( 0.000000000000000000, 0.000000000000000000, 1.000000000000000000 ) ) ;
#2607=LINE ( 'NONE', #7103, #2285 ) ;
#2616=UNCERTAINTY_MEASURE_WITH_UNIT (LENGTH_MEASURE( 1.000000000000000082E-05 ), #4951, 'distance_accuracy_value', 'NONE');
#2630=CARTESIAN_POINT ( 'NONE',  ( 2.200000000000000622, 0.000000000000000000, 2.199999999999999734 ) ) ;
#2632=DIRECTION ( 'NONE',  ( -1.000000000000000000, -0.000000000000000000, -0.000000000000000000 ) ) ;
#2639=CARTESIAN_POINT ( 'NONE',  ( 0.000000000000000000, 0.7216878364870328300, 1.250000000000000000 ) ) ;
#2640=ORIENTED_EDGE ( 'NONE', *, *, #5180, .T. ) ;
#2644=CARTESIAN_POINT ( 'NONE',  ( 2.200000000000000178, 0.000000000000000000, 3.799999999999999378 ) ) ;
#2677=CARTESIAN_POINT ( 'NONE',  ( 3.885274725274726393, -8.673617379884035472E-16, 0.000000000000000000 ) ) ;
#2681=CARTESIAN_POINT ( 'NONE',  ( 1.820000000000000062, 0.000000000000000000, 0.000000000000000000 ) ) ;
#2708=DIRECTION ( 'NONE',  ( -1.000000000000000000, 0.000000000000000000, 0.000000000000000000 ) ) ;
#2724=CARTESIAN_POINT ( 'NONE',  ( 11.80999999999999872, 0.000000000000000000, 0.000000000000000000 ) ) ;
#2728=EDGE_CURVE ( 'NONE', #3754, #2789, #7663, .T. ) ;
#2742=EDGE_LOOP ( 'NONE', ( #5941, #5386, #3180 ) ) ;
#2753=CARTESIAN_POINT ( 'NONE',  ( 2.200000000000000622, 0.000000000000000000, 0.000000000000000000 ) ) ;
#2763=FACE_OUTER_BOUND ( 'NONE', #5287, .T. ) ;
#2786=LINE ( 'NONE', #5068, #5380 ) ;
#2788=CARTESIAN_POINT ( 'NONE',  ( 0.000000000000000000, 1.443375672974065216, 1.084202172492522584E-16 ) ) ;
#2789=VERTEX_POINT ( 'NONE', #8618 ) ;
#2800=DIRECTION ( 'NONE',  ( 0.000000000000000000, 0.000000000000000000, 1.000000000000000000 ) ) ;
#2806=FACE_OUTER_BOUND ( 'NONE', #7419, .T. ) ;
#2807=DIRECTION ( 'NONE',  ( -0.000000000000000000, 1.000000000000000000, -0.000000000000000000 ) ) ;
#2822=AXIS2_PLACEMENT_3D ( 'NONE', #7850, #8491, #199 ) ;
#2830=DIRECTION ( 'NONE',  ( 0.000000000000000000, 0.000000000000000000, 1.000000000000000000 ) ) ;
#2872=DIRECTION ( 'NONE',  ( -0.7071067811865489050, 0.000000000000000000, 0.7071067811865462405 ) ) ;
#2882=LINE ( 'NONE', #1364, #5603 ) ;
#2913=LINE ( 'NONE', #329, #4360 ) ;
#2937=LINE ( 'NONE', #7391, #2507 ) ;
#2950=LINE ( 'NONE', #1579, #6192 ) ;
#2981=CIRCLE ( 'NONE', #4577, 0.2000000000000000944 ) ;
#2989=CIRCLE ( 'NONE', #3793, 2.000000000000000000 ) ;
#2992=AXIS2_PLACEMENT_3D ( 'NONE', #3134, #5376, #7694 ) ;
#3009=ORIENTED_EDGE ( 'NONE', *, *, #5108, .T. ) ;
#3011=EDGE_LOOP ( 'NONE', ( #9123, #2321, #3611, #7563 ) ) ;
#3059=CIRCLE ( 'NONE', #4340, 3.799999999999999378 ) ;
#3083=CARTESIAN_POINT ( 'NONE',  ( 2.200000000000000178, 0.000000000000000000, 0.000000000000000000 ) ) ;
#3089=APPLICATION_CONTEXT ( 'automotive_design' ) ;
#3114=EDGE_CURVE ( 'NONE', #6663, #3981, #8550, .T. ) ;
#3117=ORIENTED_EDGE ( 'NONE', *, *, #7585, .F. ) ;
#3129=ORIENTED_EDGE ( 'NONE', *, *, #7939, .F. ) ;
#3130=LINE ( 'NONE', #9127, #2447 ) ;
#3134=CARTESIAN_POINT ( 'NONE',  ( 1.300000000000000044, -0.7216878364870317197, -1.250000000000000000 ) ) ;
#3145=ORIENTED_EDGE ( 'NONE', *, *, #4319, .F. ) ;
#3180=ORIENTED_EDGE ( 'NONE', *, *, #8292, .F. ) ;
#3194=ORIENTED_EDGE ( 'NONE', *, *, #8845, .F. ) ;
#3195=CARTESIAN_POINT ( 'NONE',  ( 0.000000000000000000, 4.653657836759941744E-16, -3.799999999999999378 ) ) ;
#3200=DIRECTION ( 'NONE',  ( -1.000000000000000000, -0.000000000000000000, -0.000000000000000000 ) ) ;
#3206=EDGE_LOOP ( 'NONE', ( #3934, #6142 ) ) ;
#3217=ORIENTED_EDGE ( 'NONE', *, *, #6066, .T. ) ;
#3271=CARTESIAN_POINT ( 'NONE',  ( 8.673617379884035472E-16, 0.000000000000000000, 0.000000000000000000 ) ) ;
#3298=CARTESIAN_POINT ( 'NONE',  ( 1.300000000000000044, 1.082531754730548856, 0.6250000000000006661 ) ) ;
#3343=ORIENTED_EDGE ( 'NONE', *, *, #4278, .F. ) ;
#3377=FACE_OUTER_BOUND ( 'NONE', #601, .T. ) ;
#3381=CARTESIAN_POINT ( 'NONE',  ( 1.300000000000000044, 0.000000000000000000, 0.000000000000000000 ) ) ;
#3393=LINE ( 'NONE', #2095, #5437 ) ;
#3410=ORIENTED_EDGE ( 'NONE', *, *, #6598, .F. ) ;
#3418=CARTESIAN_POINT ( 'NONE',  ( 0.000000000000000000, 0.7216878364870328300, 1.250000000000000000 ) ) ;
#3423=DIRECTION ( 'NONE',  ( 0.000000000000000000, 0.000000000000000000, 1.000000000000000000 ) ) ;
#3428=ORIENTED_EDGE ( 'NONE', *, *, #2081, .T. ) ;
#3432=DIRECTION ( 'NONE',  ( 0.000000000000000000, 0.000000000000000000, 1.000000000000000000 ) ) ;
#3447=DIRECTION ( 'NONE',  ( -1.000000000000000000, -0.000000000000000000, -0.000000000000000000 ) ) ;
#3458=AXIS2_PLACEMENT_3D ( 'NONE', #210, #3200, #4847 ) ;
#3473=EDGE_CURVE ( 'NONE', #1358, #8367, #2950, .T. ) ;
#3475=AXIS2_PLACEMENT_3D ( 'NONE', #9752, #8220, #8773 ) ;
#3478=CARTESIAN_POINT ( 'NONE',  ( 11.80999999999999872, 0.000000000000000000, 2.000000000000000000 ) ) ;
#3479=ORIENTED_EDGE ( 'NONE', *, *, #5778, .F. ) ;
#3484=DIRECTION ( 'NONE',  ( 0.000000000000000000, 0.000000000000000000, 1.000000000000000000 ) ) ;
#3511=DIRECTION ( 'NONE',  ( 0.000000000000000000, 0.000000000000000000, -1.000000000000000000 ) ) ;
#3517=AXIS2_PLACEMENT_3D ( 'NONE', #3271, #7684, #4575 ) ;
#3518=CARTESIAN_POINT ( 'NONE',  ( 1.300000000000000044, -1.082531754730548190, -0.6250000000000002220 ) ) ;
#3526=ADVANCED_FACE ( 'NONE', ( #6157 ), #6743, .T. ) ;
#3529=PLANE ( 'NONE',  #3475 ) ;
#3532=AXIS2_PLACEMENT_3D ( 'NONE', #5623, #978, #2592 ) ;
#3533=DIRECTION ( 'NONE',  ( -1.000000000000000000, 0.000000000000000000, 0.000000000000000000 ) ) ;
#3539=DIRECTION ( 'NONE',  ( 0.000000000000000000, -0.8660254037844387076, 0.5000000000000001110 ) ) ;
#3558=VECTOR ( 'NONE', #2309, 1000.000000000000114 ) ;
#3560=CARTESIAN_POINT ( 'NONE',  ( 1.300000000000000044, 0.7216878364870328300, -1.250000000000000000 ) ) ;
#3570=DIRECTION ( 'NONE',  ( -1.000000000000000000, -0.000000000000000000, -0.000000000000000000 ) ) ;
#3590=CARTESIAN_POINT ( 'NONE',  ( 1.300000000000000044, 1.443375672974065216, 1.084202172492522584E-16 ) ) ;
#3611=ORIENTED_EDGE ( 'NONE', *, *, #7939, .T. ) ;
#3617=LINE ( 'NONE', #5935, #8286 ) ;
#3631=CARTESIAN_POINT ( 'NONE',  ( 1.300000000000000044, 1.443375672974065216, 1.084202172492522584E-16 ) ) ;
#3633=DIRECTION ( 'NONE',  ( 0.000000000000000000, 0.000000000000000000, 1.000000000000000000 ) ) ;
#3640=AXIS2_PLACEMENT_3D ( 'NONE', #1414, #1374, #2149 ) ;
#3643=VERTEX_POINT ( 'NONE', #2221 ) ;
#3662=ORIENTED_EDGE ( 'NONE', *, *, #1988, .F. ) ;
#3690=DIRECTION ( 'NONE',  ( 0.000000000000000000, 1.000000000000000000, 1.224646799147353207E-16 ) ) ;
#3717=EDGE_CURVE ( 'NONE', #2001, #3754, #933, .T. ) ;
#3733=APPLICATION_CONTEXT ( 'automotive_design' ) ;
#3746=DIRECTION ( 'NONE',  ( -0.000000000000000000, -0.5000000000000002220, 0.8660254037844384856 ) ) ;
#3747=DIRECTION ( 'NONE',  ( 0.000000000000000000, 0.000000000000000000, 1.000000000000000000 ) ) ;
#3754=VERTEX_POINT ( 'NONE', #1324 ) ;
#3793=AXIS2_PLACEMENT_3D ( 'NONE', #728, #9567, #2143 ) ;
#3808=ORIENTED_EDGE ( 'NONE', *, *, #7149, .T. ) ;
#3845=EDGE_CURVE ( 'NONE', #1276, #6854, #5026, .T. ) ;
#3876=TOROIDAL_SURFACE ( 'NONE', #1667, 2.199999999999999734, 0.2000000000000000111 ) ;
#3896=CARTESIAN_POINT ( 'NONE',  ( 1.300000000000000044, -0.7216878364870318308, 1.250000000000000000 ) ) ;
#3900=ADVANCED_FACE ( 'NONE', ( #2295 ), #9025, .T. ) ;
#3908=ORIENTED_EDGE ( 'NONE', *, *, #4619, .F. ) ;
#3934=ORIENTED_EDGE ( 'NONE', *, *, #7754, .T. ) ;
#3936=DIRECTION ( 'NONE',  ( -1.000000000000000000, -0.000000000000000000, -0.000000000000000000 ) ) ;
#3937=DIRECTION ( 'NONE',  ( 0.000000000000000000, 0.000000000000000000, 1.000000000000000000 ) ) ;
#3952=AXIS2_PLACEMENT_3D ( 'NONE', #9416, #2632, #5427 ) ;
#3956=CARTESIAN_POINT ( 'NONE',  ( 2.200000000000000178, 4.653657836759941744E-16, -3.799999999999999378 ) ) ;
#3966=FACE_BOUND ( 'NONE', #7569, .T. ) ;
#3981=VERTEX_POINT ( 'NONE', #42 ) ;
#4005=DIRECTION ( 'NONE',  ( -1.000000000000000000, 0.000000000000000000, 0.000000000000000000 ) ) ;
#4009=ADVANCED_FACE ( 'NONE', ( #4539 ), #8976, .F. ) ;
#4033=ORIENTED_EDGE ( 'NONE', *, *, #4487, .T. ) ;
#4060=ORIENTED_EDGE ( 'NONE', *, *, #5354, .T. ) ;
#4063=ORIENTED_EDGE ( 'NONE', *, *, #2728, .F. ) ;
#4078=PLANE ( 'NONE',  #7462 ) ;
#4109=ORIENTED_EDGE ( 'NONE', *, *, #7585, .T. ) ;
#4125=VERTEX_POINT ( 'NONE', #4871 ) ;
#4130=CARTESIAN_POINT ( 'NONE',  ( 8.673617379884035472E-16, 0.000000000000000000, 0.000000000000000000 ) ) ;
#4142=ADVANCED_FACE ( 'NONE', ( #8527 ), #1406, .F. ) ;
#4167=CARTESIAN_POINT ( 'NONE',  ( 1.300000000000000044, 0.000000000000000000, 0.000000000000000000 ) ) ;
#4184=CARTESIAN_POINT ( 'NONE',  ( 12.20000000000000107, 1.971681346627238735E-16, -1.610000000000000098 ) ) ;
#4199=CIRCLE ( 'NONE', #1031, 1.249999999999999778 ) ;
#4219=CARTESIAN_POINT ( 'NONE',  ( 2.400000000000000799, 2.449293598294705921E-16, -1.999999999999999556 ) ) ;
#4224=DIRECTION ( 'NONE',  ( -1.000000000000000000, -0.000000000000000000, -0.000000000000000000 ) ) ;
#4225=ORIENTED_EDGE ( 'NONE', *, *, #6237, .F. ) ;
#4231=VERTEX_POINT ( 'NONE', #5663 ) ;
#4245=DIRECTION ( 'NONE',  ( -1.000000000000000000, 0.000000000000000000, 0.000000000000000000 ) ) ;
#4255=LINE ( 'NONE', #6459, #5554 ) ;
#4257=CIRCLE ( 'NONE', #3458, 1.610000000000000098 ) ;
#4278=EDGE_CURVE ( 'NONE', #4551, #8213, #2981, .T. ) ;
#4279=LINE ( 'NONE', #2036, #6991 ) ;
#4284=LINE ( 'NONE', #8127, #7100 ) ;
#4305=CARTESIAN_POINT ( 'NONE',  ( 2.400000000000000799, 0.000000000000000000, 1.999999999999999556 ) ) ;
#4319=EDGE_CURVE ( 'NONE', #2789, #8766, #320, .T. ) ;
#4320=CARTESIAN_POINT ( 'NONE',  ( 12.20000000000000107, 0.000000000000000000, 1.610000000000000098 ) ) ;
#4324=DIRECTION ( 'NONE',  ( -0.000000000000000000, 0.5000000000000000000, 0.8660254037844385966 ) ) ;
#4340=AXIS2_PLACEMENT_3D ( 'NONE', #1523, #9725, #50 ) ;
#4346=CARTESIAN_POINT ( 'NONE',  ( 3.885274725274726393, -8.673617379884035472E-16, 0.000000000000000000 ) ) ;
#4360=VECTOR ( 'NONE', #8163, 1000.000000000000000 ) ;
#4361=CIRCLE ( 'NONE', #109, 1.249999999999999778 ) ;
#4397=DIRECTION ( 'NONE',  ( -1.000000000000000000, -0.000000000000000000, -0.000000000000000000 ) ) ;
#4402=ORIENTED_EDGE ( 'NONE', *, *, #6066, .F. ) ;
#4404=CARTESIAN_POINT ( 'NONE',  ( 0.000000000000000000, 0.7216878364870328300, -1.250000000000000000 ) ) ;
#4453=ADVANCED_BREP_SHAPE_REPRESENTATION ( '', ( #9696, #6314 ), #6474 ) ;
#4472=ORIENTED_EDGE ( 'NONE', *, *, #1950, .T. ) ;
#4473=AXIS2_PLACEMENT_3D ( 'NONE', #9600, #7475, #714 ) ;
#4481=DIRECTION ( 'NONE',  ( -1.000000000000000000, -0.000000000000000000, -0.000000000000000000 ) ) ;
#4487=EDGE_CURVE ( 'NONE', #5005, #3643, #4257, .T. ) ;
#4488=AXIS2_PLACEMENT_3D ( 'NONE', #8371, #4717, #5985 ) ;
#4518=DIRECTION ( 'NONE',  ( -0.000000000000000000, 0.000000000000000000, 1.000000000000000000 ) ) ;
#4519=AXIS2_PLACEMENT_3D ( 'NONE', #9021, #1563, #3633 ) ;
#4531=CIRCLE ( 'NONE', #8626, 1.610000000000000098 ) ;
#4539=FACE_OUTER_BOUND ( 'NONE', #607, .T. ) ;
#4543=DIRECTION ( 'NONE',  ( -1.000000000000000000, 0.000000000000000000, -0.000000000000000000 ) ) ;
#4546=CARTESIAN_POINT ( 'NONE',  ( 1.300000000000000044, 0.7216878364870328300, -1.250000000000000000 ) ) ;
#4551=VERTEX_POINT ( 'NONE', #8970 ) ;
#4564=EDGE_CURVE ( 'NONE', #9118, #4597, #5854, .T. ) ;
#4567=ORIENTED_EDGE ( 'NONE', *, *, #8185, .T. ) ;
#4571=ORIENTED_EDGE ( 'NONE', *, *, #6237, .T. ) ;
#4575=DIRECTION ( 'NONE',  ( 0.000000000000000000, 0.000000000000000000, 1.000000000000000000 ) ) ;
#4577=AXIS2_PLACEMENT_3D ( 'NONE', #5752, #7186, #7933 ) ;
#4597=VERTEX_POINT ( 'NONE', #2788 ) ;
#4602=AXIS2_PLACEMENT_3D ( 'NONE', #8142, #9079, #680 ) ;
#4603=CARTESIAN_POINT ( 'NONE',  ( 1.300000000000000044, 0.7216878364870328300, -1.250000000000000000 ) ) ;
#4619=EDGE_CURVE ( 'NONE', #1358, #6132, #2989, .T. ) ;
#4628=ADVANCED_FACE ( 'NONE', ( #7152 ), #8082, .T. ) ;
#4629=FACE_OUTER_BOUND ( 'NONE', #2742, .T. ) ;
#4643=FACE_OUTER_BOUND ( 'NONE', #5834, .T. ) ;
#4667=ORIENTED_EDGE ( 'NONE', *, *, #2239, .F. ) ;
#4686=CIRCLE ( 'NONE', #1838, 3.799999999999999378 ) ;
#4695=EDGE_CURVE ( 'NONE', #8444, #4597, #2937, .T. ) ;
#4705=DIRECTION ( 'NONE',  ( -1.000000000000000000, -0.000000000000000000, -0.000000000000000000 ) ) ;
#4717=DIRECTION ( 'NONE',  ( -1.000000000000000000, 0.000000000000000000, 0.000000000000000000 ) ) ;
#4754=CARTESIAN_POINT ( 'NONE',  ( 1.300000000000000044, -0.7216878364870317197, -1.250000000000000000 ) ) ;
#4757=EDGE_LOOP ( 'NONE', ( #3343, #3479, #5349, #4667 ) ) ;
#4783=DIRECTION ( 'NONE',  ( -1.000000000000000000, -0.000000000000000000, -0.000000000000000000 ) ) ;
#4817=ORIENTED_EDGE ( 'NONE', *, *, #5766, .F. ) ;
#4847=DIRECTION ( 'NONE',  ( 0.000000000000000000, 0.000000000000000000, 1.000000000000000000 ) ) ;
#4871=CARTESIAN_POINT ( 'NONE',  ( 1.300000000000000044, -0.7216878364870318308, 1.250000000000000000 ) ) ;
#4874=ADVANCED_FACE ( 'NONE', ( #7072 ), #1894, .T. ) ;
#4889=CARTESIAN_POINT ( 'NONE',  ( 1.300000000000000044, -1.443375672974064328, -9.326206579303807412E-18 ) ) ;
#4892=ADVANCED_FACE ( 'NONE', ( #5659 ), #5513, .T. ) ;
#4893=ORIENTED_EDGE ( 'NONE', *, *, #7972, .T. ) ;
#4896=EDGE_LOOP ( 'NONE', ( #6454, #8344, #5950 ) ) ;
#4899=CARTESIAN_POINT ( 'NONE',  ( 1.300000000000000044, 0.000000000000000000, 0.000000000000000000 ) ) ;
#4927=LINE ( 'NONE', #7941, #8515 ) ;
#4951=( LENGTH_UNIT ( ) NAMED_UNIT ( * ) SI_UNIT ( .MILLI., .METRE. ) );
#4964=DIRECTION ( 'NONE',  ( -1.000000000000000000, -0.000000000000000000, -0.000000000000000000 ) ) ;
#4989=ADVANCED_FACE ( 'NONE', ( #3377 ), #6387, .T. ) ;
#4999=DIRECTION ( 'NONE',  ( 0.000000000000000000, -0.8660254037844385966, -0.5000000000000003331 ) ) ;
#5005=VERTEX_POINT ( 'NONE', #5327 ) ;
#5012=DIRECTION ( 'NONE',  ( -1.000000000000000000, -0.000000000000000000, -0.000000000000000000 ) ) ;
#5015=CARTESIAN_POINT ( 'NONE',  ( 1.300000000000000044, 0.7216878364870328300, 1.250000000000000000 ) ) ;
#5026=LINE ( 'NONE', #1229, #8228 ) ;
#5027=CARTESIAN_POINT ( 'NONE',  ( 12.20000000000000107, 0.000000000000000000, 0.000000000000000000 ) ) ;
#5040=ADVANCED_FACE ( 'NONE', ( #2395 ), #5479, .T. ) ;
#5041=AXIS2_PLACEMENT_3D ( 'NONE', #2681, #8076, #5706 ) ;
#5049=VERTEX_POINT ( 'NONE', #7597 ) ;
#5063=ORIENTED_EDGE ( 'NONE', *, *, #7149, .F. ) ;
#5068=CARTESIAN_POINT ( 'NONE',  ( 2.021687836487040535, 0.000000000000000000, 2.168404344971008868E-16 ) ) ;
#5072=DIRECTION ( 'NONE',  ( 0.000000000000000000, 0.5000000000000001110, 0.8660254037844385966 ) ) ;
#5081=VECTOR ( 'NONE', #6898, 1000.000000000000000 ) ;
#5092=ORIENTED_EDGE ( 'NONE', *, *, #4564, .T. ) ;
#5108=EDGE_CURVE ( 'NONE', #5461, #8444, #6103, .T. ) ;
#5109=ADVANCED_FACE ( 'NONE', ( #4643 ), #7641, .T. ) ;
#5168=DIRECTION ( 'NONE',  ( 1.000000000000000000, 0.000000000000000000, 0.000000000000000000 ) ) ;
#5180=EDGE_CURVE ( 'NONE', #4125, #2236, #6439, .T. ) ;
#5191=ADVANCED_FACE ( 'NONE', ( #2585 ), #6936, .F. ) ;
#5240=AXIS2_PLACEMENT_3D ( 'NONE', #4899, #1738, #6270 ) ;
#5249=CARTESIAN_POINT ( 'NONE',  ( 2.200000000000000622, 1.999999999999999112, 0.000000000000000000 ) ) ;
#5273=ADVANCED_FACE ( 'NONE', ( #1316 ), #3529, .T. ) ;
#5278=DIRECTION ( 'NONE',  ( -1.000000000000000000, -0.000000000000000000, -0.000000000000000000 ) ) ;
#5287=EDGE_LOOP ( 'NONE', ( #8534, #2287, #2455, #1209 ) ) ;
#5294=VERTEX_POINT ( 'NONE', #7282 ) ;
#5298=ORIENTED_EDGE ( 'NONE', *, *, #5108, .F. ) ;
#5302=AXIS2_PLACEMENT_3D ( 'NONE', #4167, #461, #6460 ) ;
#5306=FACE_OUTER_BOUND ( 'NONE', #2272, .T. ) ;
#5327=CARTESIAN_POINT ( 'NONE',  ( 12.20000000000000107, 0.000000000000000000, 1.610000000000000098 ) ) ;
#5336=EDGE_LOOP ( 'NONE', ( #4571, #2524, #8701, #4109, #700, #3217 ) ) ;
#5337=EDGE_CURVE ( 'NONE', #5461, #928, #4284, .T. ) ;
#5342=ORIENTED_EDGE ( 'NONE', *, *, #4278, .T. ) ;
#5349=ORIENTED_EDGE ( 'NONE', *, *, #9609, .T. ) ;
#5354=EDGE_CURVE ( 'NONE', #5049, #6362, #2786, .T. ) ;
#5376=DIRECTION ( 'NONE',  ( 0.000000000000000000, 0.8660254037844385966, 0.5000000000000003331 ) ) ;
#5380=VECTOR ( 'NONE', #8078, 1000.000000000000114 ) ;
#5386=ORIENTED_EDGE ( 'NONE', *, *, #235, .F. ) ;
#5388=LINE ( 'NONE', #4603, #5081 ) ;
#5394=EDGE_LOOP ( 'NONE', ( #4033, #9291, #3908, #3129 ) ) ;
#5406=ORIENTED_EDGE ( 'NONE', *, *, #7972, .F. ) ;
#5418=CIRCLE ( 'NONE', #3517, 1.899999999999999689 ) ;
#5427=DIRECTION ( 'NONE',  ( 0.000000000000000000, 0.000000000000000000, 1.000000000000000000 ) ) ;
#5437=VECTOR ( 'NONE', #7346, 1000.000000000000000 ) ;
#5461=VERTEX_POINT ( 'NONE', #8472 ) ;
#5462=CIRCLE ( 'NONE', #816, 3.799999999999999378 ) ;
#5470=LINE ( 'NONE', #6928, #171 ) ;
#5471=ADVANCED_FACE ( 'NONE', ( #138 ), #2379, .T. ) ;
#5479=PLANE ( 'NONE',  #2992 ) ;
#5480=ORIENTED_EDGE ( 'NONE', *, *, #4319, .T. ) ;
#5512=EDGE_LOOP ( 'NONE', ( #1733, #9737, #5092, #866, #5298 ) ) ;
#5513=CYLINDRICAL_SURFACE ( 'NONE', #6764, 3.799999999999999378 ) ;
#5554=VECTOR ( 'NONE', #2708, 1000.000000000000000 ) ;
#5561=CARTESIAN_POINT ( 'NONE',  ( 1.820000000000000062, 0.000000000000000000, 3.799999999999999378 ) ) ;
#5562=CARTESIAN_POINT ( 'NONE',  ( -997.9783121635130101, 0.000000000000000000, 0.000000000000000000 ) ) ;
#5563=( NAMED_UNIT ( * ) PLANE_ANGLE_UNIT ( ) SI_UNIT ( $, .RADIAN. ) );
#5567=VECTOR ( 'NONE', #6203, 1000.000000000000000 ) ;
#5603=VECTOR ( 'NONE', #6588, 1000.000000000000000 ) ;
#5604=PLANE ( 'NONE',  #6817 ) ;
#5607=ORIENTED_EDGE ( 'NONE', *, *, #1184, .F. ) ;
#5623=CARTESIAN_POINT ( 'NONE',  ( -997.9783121635130101, 0.000000000000000000, 0.000000000000000000 ) ) ;
#5635=CARTESIAN_POINT ( 'NONE',  ( 1.300000000000000044, 3.252606517456513302E-16, 2.499999999999999556 ) ) ;
#5648=DIRECTION ( 'NONE',  ( -1.000000000000000000, -0.000000000000000000, -0.000000000000000000 ) ) ;
#5652=ORIENTED_EDGE ( 'NONE', *, *, #3114, .T. ) ;
#5659=FACE_OUTER_BOUND ( 'NONE', #2024, .T. ) ;
#5663=CARTESIAN_POINT ( 'NONE',  ( 1.300000000000000044, -1.082531754730548190, 0.6250000000000000000 ) ) ;
#5666=DIRECTION ( 'NONE',  ( -0.000000000000000000, -0.5000000000000002220, 0.8660254037844384856 ) ) ;
#5670=FACE_OUTER_BOUND ( 'NONE', #5512, .T. ) ;
#5678=AXIS2_PLACEMENT_3D ( 'NONE', #2677, #9464, #1942 ) ;
#5690=CARTESIAN_POINT ( 'NONE',  ( 0.000000000000000000, -0.7216878364870317197, -1.250000000000000000 ) ) ;
#5698=DIRECTION ( 'NONE',  ( -1.000000000000000000, -0.000000000000000000, -0.000000000000000000 ) ) ;
#5706=DIRECTION ( 'NONE',  ( 0.000000000000000000, 0.000000000000000000, 1.000000000000000000 ) ) ;
#5709=AXIS2_PLACEMENT_3D ( 'NONE', #2185, #6041, #7638 ) ;
#5750=VERTEX_POINT ( 'NONE', #633 ) ;
#5752=CARTESIAN_POINT ( 'NONE',  ( 2.400000000000000799, 2.694222958124176513E-16, -2.199999999999999734 ) ) ;
#5760=ADVANCED_FACE ( 'NONE', ( #2150, #8143 ), #7493, .T. ) ;
#5766=EDGE_CURVE ( 'NONE', #2789, #6478, #1952, .T. ) ;
#5778=EDGE_CURVE ( 'NONE', #7854, #4551, #1333, .T. ) ;
#5818=VECTOR ( 'NONE', #9605, 1000.000000000000000 ) ;
#5834=EDGE_LOOP ( 'NONE', ( #8628, #8795, #2640, #4225, #6911 ) ) ;
#5854=LINE ( 'NONE', #3631, #9620 ) ;
#5869=DIRECTION ( 'NONE',  ( -1.000000000000000000, -0.000000000000000000, -0.000000000000000000 ) ) ;
#5878=FACE_OUTER_BOUND ( 'NONE', #5891, .T. ) ;
#5891=EDGE_LOOP ( 'NONE', ( #4817, #5480, #391, #4893, #2312 ) ) ;
#5920=CARTESIAN_POINT ( 'NONE',  ( 0.000000000000000000, 0.000000000000000000, 0.000000000000000000 ) ) ;
#5935=CARTESIAN_POINT ( 'NONE',  ( 0.000000000000000000, 0.000000000000000000, 3.799999999999999378 ) ) ;
#5941=ORIENTED_EDGE ( 'NONE', *, *, #273, .F. ) ;
#5950=ORIENTED_EDGE ( 'NONE', *, *, #8842, .F. ) ;
#5985=DIRECTION ( 'NONE',  ( 0.000000000000000000, 0.000000000000000000, 1.000000000000000000 ) ) ;
#6006=AXIS2_PLACEMENT_3D ( 'NONE', #696, #4999, #9535 ) ;
#6010=EDGE_LOOP ( 'NONE', ( #7955, #2367, #562 ) ) ;
#6037=ORIENTED_EDGE ( 'NONE', *, *, #9093, .F. ) ;
#6041=DIRECTION ( 'NONE',  ( -1.000000000000000000, -0.000000000000000000, -0.000000000000000000 ) ) ;
#6045=DIRECTION ( 'NONE',  ( 0.000000000000000000, 0.000000000000000000, 1.000000000000000000 ) ) ;
#6054=EDGE_LOOP ( 'NONE', ( #7958, #6230, #8348, #718 ) ) ;
#6066=EDGE_CURVE ( 'NONE', #4597, #6854, #9426, .T. ) ;
#6103=LINE ( 'NONE', #2343, #176 ) ;
#6114=CARTESIAN_POINT ( 'NONE',  ( 0.000000000000000000, -0.7216878364870317197, -1.250000000000000000 ) ) ;
#6132=VERTEX_POINT ( 'NONE', #7082 ) ;
#6142=ORIENTED_EDGE ( 'NONE', *, *, #7743, .T. ) ;
#6148=DIRECTION ( 'NONE',  ( -1.000000000000000000, 0.000000000000000000, 0.000000000000000000 ) ) ;
#6157=FACE_OUTER_BOUND ( 'NONE', #7560, .T. ) ;
#6169=AXIS2_PLACEMENT_3D ( 'NONE', #1459, #1413, #6736 ) ;
#6188=AXIS2_PLACEMENT_3D ( 'NONE', #2724, #5698, #3432 ) ;
#6192=VECTOR ( 'NONE', #5278, 1000.000000000000000 ) ;
#6203=DIRECTION ( 'NONE',  ( -1.000000000000000000, -0.000000000000000000, -0.000000000000000000 ) ) ;
#6209=LINE ( 'NONE', #6114, #3558 ) ;
#6216=ORIENTED_EDGE ( 'NONE', *, *, #9427, .F. ) ;
#6230=ORIENTED_EDGE ( 'NONE', *, *, #1012, .T. ) ;
#6237=EDGE_CURVE ( 'NONE', #6854, #2236, #2882, .T. ) ;
#6270=DIRECTION ( 'NONE',  ( 0.000000000000000000, 0.000000000000000000, 1.000000000000000000 ) ) ;
#6314=AXIS2_PLACEMENT_3D ( 'NONE', #9654, #2830, #5168 ) ;
#6335=FACE_OUTER_BOUND ( 'NONE', #4896, .T. ) ;
#6362=VERTEX_POINT ( 'NONE', #2333 ) ;
#6367=ADVANCED_FACE ( 'NONE', ( #4629 ), #9167, .T. ) ;
#6370=LINE ( 'NONE', #416, #261 ) ;
#6387=CYLINDRICAL_SURFACE ( 'NONE', #3952, 3.799999999999999378 ) ;
#6389=AXIS2_PLACEMENT_3D ( 'NONE', #869, #6877, #2380 ) ;
#6406=VERTEX_POINT ( 'NONE', #7173 ) ;
#6428=ORIENTED_EDGE ( 'NONE', *, *, #2229, .F. ) ;
#6431=DIRECTION ( 'NONE',  ( 0.000000000000000000, 0.000000000000000000, 1.000000000000000000 ) ) ;
#6439=LINE ( 'NONE', #9316, #803 ) ;
#6454=ORIENTED_EDGE ( 'NONE', *, *, #1473, .F. ) ;
#6459=CARTESIAN_POINT ( 'NONE',  ( 1.300000000000000044, -0.7216878364870317197, -1.250000000000000000 ) ) ;
#6460=DIRECTION ( 'NONE',  ( 0.000000000000000000, 0.000000000000000000, 1.000000000000000000 ) ) ;
#6462=( NAMED_UNIT ( * ) SI_UNIT ( $, .STERADIAN. ) SOLID_ANGLE_UNIT ( ) );
#6474=( GEOMETRIC_REPRESENTATION_CONTEXT ( 3 ) GLOBAL_UNCERTAINTY_ASSIGNED_CONTEXT ( ( #2616 ) ) GLOBAL_UNIT_ASSIGNED_CONTEXT ( ( #4951, #7368, #6462 ) ) REPRESENTATION_CONTEXT ( 'NONE', 'WORKASPACE' ) );
#6478=VERTEX_POINT ( 'NONE', #8567 ) ;
#6506=AXIS2_PLACEMENT_3D ( 'NONE', #4130, #5012, #6431 ) ;
#6512=VECTOR ( 'NONE', #4397, 1000.000000000000000 ) ;
#6519=DIRECTION ( 'NONE',  ( 0.000000000000000000, 1.000000000000000000, 0.000000000000000000 ) ) ;
#6548=DIRECTION ( 'NONE',  ( 0.000000000000000000, -0.5000000000000000000, -0.8660254037844385966 ) ) ;
#6588=DIRECTION ( 'NONE',  ( -0.000000000000000000, -1.000000000000000000, -0.000000000000000000 ) ) ;
#6596=CARTESIAN_POINT ( 'NONE',  ( 4.336808689942017736E-16, 0.000000000000000000, 0.000000000000000000 ) ) ;
#6598=EDGE_CURVE ( 'NONE', #9443, #8766, #3617, .T. ) ;
#6631=PRODUCT_DEFINITION_FORMATION_WITH_SPECIFIED_SOURCE ( 'ANY', '', #2350, .NOT_KNOWN. ) ;
#6633=ORIENTED_EDGE ( 'NONE', *, *, #2488, .T. ) ;
#6652=DIRECTION ( 'NONE',  ( -1.000000000000000000, -0.000000000000000000, -0.000000000000000000 ) ) ;
#6657=ORIENTED_EDGE ( 'NONE', *, *, #9459, .F. ) ;
#6663=VERTEX_POINT ( 'NONE', #3518 ) ;
#6684=CARTESIAN_POINT ( 'NONE',  ( 1.820000000000000062, 0.000000000000000000, 0.000000000000000000 ) ) ;
#6705=ADVANCED_FACE ( 'NONE', ( #572 ), #9556, .T. ) ;
#6731=DIRECTION ( 'NONE',  ( -0.000000000000000000, 0.5000000000000000000, 0.8660254037844385966 ) ) ;
#6736=DIRECTION ( 'NONE',  ( -0.000000000000000000, 0.000000000000000000, 1.000000000000000000 ) ) ;
#6743=PLANE ( 'NONE',  #9507 ) ;
#6764=AXIS2_PLACEMENT_3D ( 'NONE', #8523, #4964, #7883 ) ;
#6779=DIRECTION ( 'NONE',  ( -0.000000000000000000, -1.000000000000000000, -0.000000000000000000 ) ) ;
#6788=ADVANCED_FACE ( 'NONE', ( #3966, #5306 ), #2212, .F. ) ;
#6795=DIRECTION ( 'NONE',  ( 1.000000000000000000, 0.000000000000000000, 0.000000000000000000 ) ) ;
#6807=VECTOR ( 'NONE', #1011, 1000.000000000000000 ) ;
#6817=AXIS2_PLACEMENT_3D ( 'NONE', #7881, #7832, #9413 ) ;
#6837=AXIS2_PLACEMENT_3D ( 'NONE', #3590, #3539, #6548 ) ;
#6845=CARTESIAN_POINT ( 'NONE',  ( 4.336808689942017736E-16, -0.7216878364870318308, 1.250000000000000000 ) ) ;
#6854=VERTEX_POINT ( 'NONE', #3418 ) ;
#6865=ORIENTED_EDGE ( 'NONE', *, *, #5354, .F. ) ;
#6877=DIRECTION ( 'NONE',  ( -1.000000000000000000, 0.000000000000000000, 0.000000000000000000 ) ) ;
#6898=DIRECTION ( 'NONE',  ( -0.000000000000000000, 1.000000000000000000, -0.000000000000000000 ) ) ;
#6911=ORIENTED_EDGE ( 'NONE', *, *, #3845, .F. ) ;
#6916=ORIENTED_EDGE ( 'NONE', *, *, #3845, .T. ) ;
#6925=EDGE_CURVE ( 'NONE', #8659, #928, #1758, .T. ) ;
#6928=CARTESIAN_POINT ( 'NONE',  ( 1.300000000000000044, -1.443375672974064328, -9.326206579303807412E-18 ) ) ;
#6936=TOROIDAL_SURFACE ( 'NONE', #8206, 2.199999999999999734, 0.2000000000000000111 ) ;
#6940=ORIENTED_EDGE ( 'NONE', *, *, #8292, .T. ) ;
#6957=DIRECTION ( 'NONE',  ( 0.000000000000000000, 0.000000000000000000, 1.000000000000000000 ) ) ;
#6981=( LENGTH_UNIT ( ) NAMED_UNIT ( * ) SI_UNIT ( .MILLI., .METRE. ) );
#6991=VECTOR ( 'NONE', #4324, 1000.000000000000227 ) ;
#7027=ORIENTED_EDGE ( 'NONE', *, *, #8430, .F. ) ;
#7036=ADVANCED_FACE ( 'NONE', ( #2806 ), #7459, .T. ) ;
#7042=DIRECTION ( 'NONE',  ( -1.000000000000000000, -0.000000000000000000, -0.000000000000000000 ) ) ;
#7069=DIRECTION ( 'NONE',  ( 0.000000000000000000, 0.000000000000000000, 1.000000000000000000 ) ) ;
#7072=FACE_OUTER_BOUND ( 'NONE', #7488, .T. ) ;
#7082=CARTESIAN_POINT ( 'NONE',  ( 11.80999999999999872, 2.449293598294706414E-16, -2.000000000000000000 ) ) ;
#7087=EDGE_CURVE ( 'NONE', #3981, #1595, #4255, .T. ) ;
#7100=VECTOR ( 'NONE', #7336, 1000.000000000000227 ) ;
#7103=CARTESIAN_POINT ( 'NONE',  ( 1.300000000000000044, 0.7216878364870328300, 1.250000000000000000 ) ) ;
#7104=( GEOMETRIC_REPRESENTATION_CONTEXT ( 3 ) GLOBAL_UNCERTAINTY_ASSIGNED_CONTEXT ( ( #9010 ) ) GLOBAL_UNIT_ASSIGNED_CONTEXT ( ( #6981, #5563, #1022 ) ) REPRESENTATION_CONTEXT ( 'NONE', 'WORKASPACE' ) );
#7124=DIRECTION ( 'NONE',  ( -1.000000000000000000, 0.000000000000000000, 0.000000000000000000 ) ) ;
#7137=CIRCLE ( 'NONE', #4473, 4.324969328314201888 ) ;
#7144=EDGE_LOOP ( 'NONE', ( #9052, #4060, #2452, #1712, #1013 ) ) ;
#7149=EDGE_CURVE ( 'NONE', #3981, #8583, #5388, .T. ) ;
#7152=FACE_OUTER_BOUND ( 'NONE', #9089, .T. ) ;
#7162=PRODUCT_DEFINITION_CONTEXT ( 'detailed design', #3733, 'design' ) ;
#7164=AXIS2_PLACEMENT_3D ( 'NONE', #7450, #6795, #3747 ) ;
#7173=CARTESIAN_POINT ( 'NONE',  ( 1.300000000000000044, -1.443375672974064328, -9.326206579303807412E-18 ) ) ;
#7186=DIRECTION ( 'NONE',  ( -0.000000000000000000, 1.000000000000000000, 1.224646799147353207E-16 ) ) ;
#7244=DIRECTION ( 'NONE',  ( 0.000000000000000000, 0.000000000000000000, 1.000000000000000000 ) ) ;
#7282=CARTESIAN_POINT ( 'NONE',  ( 8.673617379884035472E-16, 1.899999999999999689, 0.000000000000000000 ) ) ;
#7336=DIRECTION ( 'NONE',  ( -0.000000000000000000, 0.5000000000000000000, 0.8660254037844385966 ) ) ;
#7346=DIRECTION ( 'NONE',  ( -0.000000000000000000, -0.5000000000000001110, -0.8660254037844385966 ) ) ;
#7354=CARTESIAN_POINT ( 'NONE',  ( 2.200000000000000622, 0.000000000000000000, 0.000000000000000000 ) ) ;
#7368=( NAMED_UNIT ( * ) PLANE_ANGLE_UNIT ( ) SI_UNIT ( $, .RADIAN. ) );
#7391=CARTESIAN_POINT ( 'NONE',  ( 0.000000000000000000, 1.443375672974065216, 1.084202172492522584E-16 ) ) ;
#7406=VERTEX_POINT ( 'NONE', #8542 ) ;
#7419=EDGE_LOOP ( 'NONE', ( #4472, #787, #6916, #4402, #170 ) ) ;
#7432=ORIENTED_EDGE ( 'NONE', *, *, #3717, .T. ) ;
#7450=CARTESIAN_POINT ( 'NONE',  ( 2.400000000000000799, 0.000000000000000000, 0.000000000000000000 ) ) ;
#7452=DIRECTION ( 'NONE',  ( 0.000000000000000000, 0.000000000000000000, 1.000000000000000000 ) ) ;
#7459=PLANE ( 'NONE',  #6006 ) ;
#7462=AXIS2_PLACEMENT_3D ( 'NONE', #1940, #7124, #7069 ) ;
#7465=SHAPE_DEFINITION_REPRESENTATION ( #1577, #490 ) ;
#7471=CARTESIAN_POINT ( 'NONE',  ( 1.300000000000000044, -0.7216878364870318308, 1.250000000000000000 ) ) ;
#7475=DIRECTION ( 'NONE',  ( 0.000000000000000000, 0.000000000000000000, 1.000000000000000000 ) ) ;
#7483=CONICAL_SURFACE ( 'NONE', #3532, 1732.050807568856271, 1.047197551196592524 ) ;
#7488=EDGE_LOOP ( 'NONE', ( #1145, #9584, #7770, #1337, #5406 ) ) ;
#7493=PLANE ( 'NONE',  #9533 ) ;
#7498=CIRCLE ( 'NONE', #5302, 1.249999999999999778 ) ;
#7560=EDGE_LOOP ( 'NONE', ( #3808, #8951, #3009, #3117, #9305 ) ) ;
#7563=ORIENTED_EDGE ( 'NONE', *, *, #7774, .F. ) ;
#7569=EDGE_LOOP ( 'NONE', ( #2359, #3428 ) ) ;
#7585=EDGE_CURVE ( 'NONE', #1595, #8444, #1702, .T. ) ;
#7586=CARTESIAN_POINT ( 'NONE',  ( 0.000000000000000000, 0.7216878364870328300, -1.250000000000000000 ) ) ;
#7594=CARTESIAN_POINT ( 'NONE',  ( 1.300000000000000044, 0.000000000000000000, 0.000000000000000000 ) ) ;
#7597=CARTESIAN_POINT ( 'NONE',  ( 2.021687836487040535, 2.168404344971008868E-16, 0.000000000000000000 ) ) ;
#7638=DIRECTION ( 'NONE',  ( 0.000000000000000000, 0.000000000000000000, 1.000000000000000000 ) ) ;
#7641=PLANE ( 'NONE',  #492 ) ;
#7663=CIRCLE ( 'NONE', #417, 3.799999999999999378 ) ;
#7684=DIRECTION ( 'NONE',  ( -1.000000000000000000, -0.000000000000000000, -0.000000000000000000 ) ) ;
#7694=DIRECTION ( 'NONE',  ( 0.000000000000000000, -0.5000000000000002220, 0.8660254037844384856 ) ) ;
#7743=EDGE_CURVE ( 'NONE', #6478, #5294, #5418, .T. ) ;
#7754=EDGE_CURVE ( 'NONE', #5294, #6478, #1463, .T. ) ;
#7770=ORIENTED_EDGE ( 'NONE', *, *, #5766, .T. ) ;
#7774=EDGE_CURVE ( 'NONE', #6132, #1358, #682, .T. ) ;
#7785=DIRECTION ( 'NONE',  ( 0.000000000000000000, 0.000000000000000000, 1.000000000000000000 ) ) ;
#7807=ORIENTED_EDGE ( 'NONE', *, *, #6598, .T. ) ;
#7810=ADVANCED_FACE ( 'NONE', ( #2573 ), #5604, .T. ) ;
#7832=DIRECTION ( 'NONE',  ( -1.000000000000000000, 0.000000000000000000, 0.000000000000000000 ) ) ;
#7833=ADVANCED_FACE ( 'NONE', ( #6335 ), #4078, .T. ) ;
#7850=CARTESIAN_POINT ( 'NONE',  ( 2.200000000000000178, 0.000000000000000000, 0.000000000000000000 ) ) ;
#7854=VERTEX_POINT ( 'NONE', #2630 ) ;
#7881=CARTESIAN_POINT ( 'NONE',  ( 1.300000000000000044, 3.252606517456513302E-16, 2.499999999999999556 ) ) ;
#7883=DIRECTION ( 'NONE',  ( 0.000000000000000000, 0.000000000000000000, 1.000000000000000000 ) ) ;
#7890=DIRECTION ( 'NONE',  ( -1.000000000000000000, 0.000000000000000000, 0.000000000000000000 ) ) ;
#7896=AXIS2_PLACEMENT_3D ( 'NONE', #4889, #7907, #5072 ) ;
#7897=PLANE ( 'NONE',  #6837 ) ;
#7907=DIRECTION ( 'NONE',  ( 0.000000000000000000, 0.8660254037844385966, -0.5000000000000001110 ) ) ;
#7917=SHAPE_REPRESENTATION_RELATIONSHIP ( 'NONE' , 'NONE' ,  #490, #4453 ) ;
#7933=DIRECTION ( 'NONE',  ( 0.000000000000000000, -1.224646799147353207E-16, 1.000000000000000000 ) ) ;
#7939=EDGE_CURVE ( 'NONE', #5005, #1358, #664, .T. ) ;
#7941=CARTESIAN_POINT ( 'NONE',  ( 1.300000000000000044, -0.7216878364870318308, 1.250000000000000000 ) ) ;
#7955=ORIENTED_EDGE ( 'NONE', *, *, #1950, .F. ) ;
#7958=ORIENTED_EDGE ( 'NONE', *, *, #4619, .T. ) ;
#7972=EDGE_CURVE ( 'NONE', #7406, #5294, #7137, .T. ) ;
#8015=SPHERICAL_SURFACE ( 'NONE', #1728, 4.324969328314201888 ) ;
#8039=CIRCLE ( 'NONE', #2822, 3.799999999999999378 ) ;
#8057=CIRCLE ( 'NONE', #3640, 0.2000000000000000944 ) ;
#8076=DIRECTION ( 'NONE',  ( -1.000000000000000000, -0.000000000000000000, -0.000000000000000000 ) ) ;
#8078=DIRECTION ( 'NONE',  ( -0.5000000000000044409, 0.000000000000000000, 0.8660254037844360431 ) ) ;
#8082=PLANE ( 'NONE',  #7896 ) ;
#8101=ORIENTED_EDGE ( 'NONE', *, *, #8845, .T. ) ;
#8127=CARTESIAN_POINT ( 'NONE',  ( 1.300000000000000044, 1.443375672974065216, 1.084202172492522584E-16 ) ) ;
#8142=CARTESIAN_POINT ( 'NONE',  ( 0.000000000000000000, 0.000000000000000000, 0.000000000000000000 ) ) ;
#8143=FACE_BOUND ( 'NONE', #5336, .T. ) ;
#8144=VECTOR ( 'NONE', #9741, 1000.000000000000000 ) ;
#8163=DIRECTION ( 'NONE',  ( -1.000000000000000000, 0.000000000000000000, 0.000000000000000000 ) ) ;
#8185=EDGE_CURVE ( 'NONE', #5049, #8583, #6370, .T. ) ;
#8205=LINE ( 'NONE', #7471, #8144 ) ;
#8206=AXIS2_PLACEMENT_3D ( 'NONE', #485, #4783, #3484 ) ;
#8213=VERTEX_POINT ( 'NONE', #4219 ) ;
#8220=DIRECTION ( 'NONE',  ( -1.000000000000000000, 0.000000000000000000, 0.000000000000000000 ) ) ;
#8228=VECTOR ( 'NONE', #4245, 1000.000000000000000 ) ;
#8260=DIRECTION ( 'NONE',  ( -1.000000000000000000, 0.000000000000000000, -0.000000000000000000 ) ) ;
#8263=ORIENTED_EDGE ( 'NONE', *, *, #5180, .F. ) ;
#8282=FACE_OUTER_BOUND ( 'NONE', #6054, .T. ) ;
#8286=VECTOR ( 'NONE', #8957, 1000.000000000000000 ) ;
#8292=EDGE_CURVE ( 'NONE', #4231, #6362, #7498, .T. ) ;
#8319=LINE ( 'NONE', #1552, #262 ) ;
#8344=ORIENTED_EDGE ( 'NONE', *, *, #2488, .F. ) ;
#8348=ORIENTED_EDGE ( 'NONE', *, *, #2239, .T. ) ;
#8367=VERTEX_POINT ( 'NONE', #4305 ) ;
#8371=CARTESIAN_POINT ( 'NONE',  ( 1.300000000000000044, 3.252606517456513302E-16, 2.499999999999999556 ) ) ;
#8376=ADVANCED_FACE ( 'NONE', ( #2763 ), #1431, .T. ) ;
#8419=ADVANCED_FACE ( 'NONE', ( #9732 ), #3876, .F. ) ;
#8430=EDGE_CURVE ( 'NONE', #8583, #5461, #9676, .T. ) ;
#8444=VERTEX_POINT ( 'NONE', #4404 ) ;
#8472=CARTESIAN_POINT ( 'NONE',  ( 1.300000000000000044, 0.7216878364870328300, -1.250000000000000000 ) ) ;
#8479=DIRECTION ( 'NONE',  ( -0.000000000000000000, -0.5000000000000001110, -0.8660254037844385966 ) ) ;
#8483=DIRECTION ( 'NONE',  ( -1.000000000000000000, -0.000000000000000000, -0.000000000000000000 ) ) ;
#8491=DIRECTION ( 'NONE',  ( -1.000000000000000000, -0.000000000000000000, -0.000000000000000000 ) ) ;
#8503=FACE_OUTER_BOUND ( 'NONE', #1680, .T. ) ;
#8515=VECTOR ( 'NONE', #6779, 1000.000000000000000 ) ;
#8520=EDGE_CURVE ( 'NONE', #5750, #1595, #6209, .T. ) ;
#8523=CARTESIAN_POINT ( 'NONE',  ( 0.000000000000000000, 0.000000000000000000, 0.000000000000000000 ) ) ;
#8527=FACE_OUTER_BOUND ( 'NONE', #7144, .T. ) ;
#8534=ORIENTED_EDGE ( 'NONE', *, *, #1012, .F. ) ;
#8542=CARTESIAN_POINT ( 'NONE',  ( 1.820000000000000062, 3.799999999999999378, 0.000000000000000000 ) ) ;
#8550=LINE ( 'NONE', #4754, #1809 ) ;
#8567=CARTESIAN_POINT ( 'NONE',  ( 8.673617379884035472E-16, -1.899999999999999689, -3.490243377569955075E-16 ) ) ;
#8583=VERTEX_POINT ( 'NONE', #940 ) ;
#8618=CARTESIAN_POINT ( 'NONE',  ( 1.820000000000000062, -3.800000000000000266, -4.653657836759940757E-16 ) ) ;
#8626=AXIS2_PLACEMENT_3D ( 'NONE', #5027, #3447, #8785 ) ;
#8627=CLOSED_SHELL ( 'NONE', ( #2403, #5191, #3900, #9627, #4892, #4874, #5760, #34, #4989, #6788, #8376, #6705, #4009, #8419, #4628, #5040, #3526, #2523, #7036, #5109, #1965, #5471, #7810, #5273, #7833, #6367, #4142 ) ) ;
#8628=ORIENTED_EDGE ( 'NONE', *, *, #9093, .T. ) ;
#8650=CARTESIAN_POINT ( 'NONE',  ( 1.300000000000000044, 1.443375672974065216, 1.084202172492522584E-16 ) ) ;
#8659=VERTEX_POINT ( 'NONE', #3298 ) ;
#8677=DIRECTION ( 'NONE',  ( -1.000000000000000000, 0.000000000000000000, -0.000000000000000000 ) ) ;
#8701=ORIENTED_EDGE ( 'NONE', *, *, #8520, .T. ) ;
#8740=CARTESIAN_POINT ( 'NONE',  ( 0.000000000000000000, 2.449293598294705921E-16, -1.999999999999999556 ) ) ;
#8766=VERTEX_POINT ( 'NONE', #5561 ) ;
#8770=CARTESIAN_POINT ( 'NONE',  ( 1.300000000000000044, 1.082531754730548856, -0.6250000000000002220 ) ) ;
#8773=DIRECTION ( 'NONE',  ( 0.000000000000000000, 0.000000000000000000, 1.000000000000000000 ) ) ;
#8776=EDGE_CURVE ( 'NONE', #8583, #6663, #2132, .T. ) ;
#8785=DIRECTION ( 'NONE',  ( 0.000000000000000000, 0.000000000000000000, 1.000000000000000000 ) ) ;
#8795=ORIENTED_EDGE ( 'NONE', *, *, #235, .T. ) ;
#8813=ORIENTED_EDGE ( 'NONE', *, *, #7087, .T. ) ;
#8814=LINE ( 'NONE', #4184, #5818 ) ;
#8842=EDGE_CURVE ( 'NONE', #6663, #4231, #1834, .T. ) ;
#8845=EDGE_CURVE ( 'NONE', #6406, #5750, #2913, .T. ) ;
#8951=ORIENTED_EDGE ( 'NONE', *, *, #8430, .T. ) ;
#8957=DIRECTION ( 'NONE',  ( -1.000000000000000000, -0.000000000000000000, -0.000000000000000000 ) ) ;
#8970=CARTESIAN_POINT ( 'NONE',  ( 2.200000000000000622, 2.694222958124176513E-16, -2.199999999999999734 ) ) ;
#8976=PLANE ( 'NONE',  #6169 ) ;
#9010=UNCERTAINTY_MEASURE_WITH_UNIT (LENGTH_MEASURE( 1.000000000000000082E-05 ), #6981, 'distance_accuracy_value', 'NONE');
#9021=CARTESIAN_POINT ( 'NONE',  ( 2.400000000000000799, 0.000000000000000000, 0.000000000000000000 ) ) ;
#9025=CONICAL_SURFACE ( 'NONE', #5709, 1.610000000000000098, 0.7853981633974463916 ) ;
#9052=ORIENTED_EDGE ( 'NONE', *, *, #8185, .F. ) ;
#9079=DIRECTION ( 'NONE',  ( -1.000000000000000000, -0.000000000000000000, -0.000000000000000000 ) ) ;
#9087=AXIS2_PLACEMENT_3D ( 'NONE', #5635, #4005, #212 ) ;
#9089=EDGE_LOOP ( 'NONE', ( #9637, #6633, #8101, #1086, #8263 ) ) ;
#9093=EDGE_CURVE ( 'NONE', #1276, #6362, #8205, .T. ) ;
#9116=DIRECTION ( 'NONE',  ( -0.000000000000000000, 0.5000000000000002220, -0.8660254037844384856 ) ) ;
#9118=VERTEX_POINT ( 'NONE', #8650 ) ;
#9123=ORIENTED_EDGE ( 'NONE', *, *, #952, .F. ) ;
#9127=CARTESIAN_POINT ( 'NONE',  ( 0.000000000000000000, -1.443375672974064328, -9.326206579303807412E-18 ) ) ;
#9167=PLANE ( 'NONE',  #6389 ) ;
#9198=CARTESIAN_POINT ( 'NONE',  ( 1.300000000000000044, 0.000000000000000000, 0.000000000000000000 ) ) ;
#9222=ORIENTED_EDGE ( 'NONE', *, *, #2081, .F. ) ;
#9290=DIRECTION ( 'NONE',  ( -0.000000000000000000, -0.5000000000000002220, 0.8660254037844384856 ) ) ;
#9291=ORIENTED_EDGE ( 'NONE', *, *, #952, .T. ) ;
#9305=ORIENTED_EDGE ( 'NONE', *, *, #7087, .F. ) ;
#9316=CARTESIAN_POINT ( 'NONE',  ( 1.300000000000000044, -0.7216878364870318308, 1.250000000000000000 ) ) ;
#9321=ORIENTED_EDGE ( 'NONE', *, *, #412, .F. ) ;
#9323=ORIENTED_EDGE ( 'NONE', *, *, #3114, .F. ) ;
#9413=DIRECTION ( 'NONE',  ( 0.000000000000000000, 0.000000000000000000, 1.000000000000000000 ) ) ;
#9416=CARTESIAN_POINT ( 'NONE',  ( 0.000000000000000000, 0.000000000000000000, 0.000000000000000000 ) ) ;
#9421=DIRECTION ( 'NONE',  ( 0.000000000000000000, 0.000000000000000000, 1.000000000000000000 ) ) ;
#9426=LINE ( 'NONE', #2639, #879 ) ;
#9427=EDGE_CURVE ( 'NONE', #7406, #3754, #4686, .T. ) ;
#9443=VERTEX_POINT ( 'NONE', #2644 ) ;
#9449=CARTESIAN_POINT ( 'NONE',  ( 1.300000000000000044, 0.7216878364870328300, 1.250000000000000000 ) ) ;
#9459=EDGE_CURVE ( 'NONE', #3643, #5005, #4531, .T. ) ;
#9464=DIRECTION ( 'NONE',  ( 0.000000000000000000, 0.000000000000000000, -1.000000000000000000 ) ) ;
#9507=AXIS2_PLACEMENT_3D ( 'NONE', #4546, #7452, #4 ) ;
#9533=AXIS2_PLACEMENT_3D ( 'NONE', #6596, #4543, #46 ) ;
#9535=DIRECTION ( 'NONE',  ( 0.000000000000000000, 0.5000000000000002220, -0.8660254037844384856 ) ) ;
#9556=CONICAL_SURFACE ( 'NONE', #1508, 1.610000000000000098, 0.7853981633974463916 ) ;
#9567=DIRECTION ( 'NONE',  ( -1.000000000000000000, -0.000000000000000000, -0.000000000000000000 ) ) ;
#9584=ORIENTED_EDGE ( 'NONE', *, *, #2728, .T. ) ;
#9599=CARTESIAN_POINT ( 'NONE',  ( 12.20000000000000107, 0.000000000000000000, 0.000000000000000000 ) ) ;
#9600=CARTESIAN_POINT ( 'NONE',  ( 3.885274725274726393, -8.673617379884035472E-16, 0.000000000000000000 ) ) ;
#9605=DIRECTION ( 'NONE',  ( -0.7071067811865489050, 8.659560562354915602E-17, -0.7071067811865462405 ) ) ;
#9609=EDGE_CURVE ( 'NONE', #7854, #8367, #8057, .T. ) ;
#9620=VECTOR ( 'NONE', #3533, 1000.000000000000000 ) ;
#9627=ADVANCED_FACE ( 'NONE', ( #8282 ), #43, .T. ) ;
#9637=ORIENTED_EDGE ( 'NONE', *, *, #273, .T. ) ;
#9654=CARTESIAN_POINT ( 'NONE',  ( 0.000000000000000000, 0.000000000000000000, 0.000000000000000000 ) ) ;
#9676=LINE ( 'NONE', #3560, #102 ) ;
#9685=ORIENTED_EDGE ( 'NONE', *, *, #8776, .T. ) ;
#9696=MANIFOLD_SOLID_BREP ( 'Hex', #8627 ) ;
#9725=DIRECTION ( 'NONE',  ( -1.000000000000000000, -0.000000000000000000, -0.000000000000000000 ) ) ;
#9732=FACE_OUTER_BOUND ( 'NONE', #4757, .T. ) ;
#9735=PRODUCT_CONTEXT ( 'NONE', #3089, 'mechanical' ) ;
#9737=ORIENTED_EDGE ( 'NONE', *, *, #1249, .T. ) ;
#9741=DIRECTION ( 'NONE',  ( -0.000000000000000000, -1.000000000000000000, -0.000000000000000000 ) ) ;
#9752=CARTESIAN_POINT ( 'NONE',  ( 1.300000000000000044, 3.252606517456513302E-16, 2.499999999999999556 ) ) ;
#9793=COLOUR_RGB('Black',0.12,0.14,0.17);
#9794=FILL_AREA_STYLE_COLOUR('',#9793);
#9795=FILL_AREA_STYLE('',(#9794));
#9796=SURFACE_STYLE_FILL_AREA(#9795);
#9797=SURFACE_SIDE_STYLE('',(#9796));
#9798=SURFACE_STYLE_USAGE(.BOTH.,#9797);
#9799=PRESENTATION_STYLE_ASSIGNMENT((#9798));
ENDSEC;
END-ISO-10303-21;
